ISO-10303-21;
HEADER;
/* Generated by software containing ST-Developer
 * from STEP Tools, Inc. (www.steptools.com) 
 */

FILE_DESCRIPTION(
/* description */ ('Belt tensioner idler arm'),
/* implementation_level */ '2;1');

FILE_NAME(
/* name */ 'Flat Washer - M5.step',
/* time_stamp */ '2026-10-28T03:22:15-07:00',
/* author */ (''),
/* organization */ (''),
/* preprocessor_version */ 'ST-DEVELOPER v20.2',
/* originating_system */ 'Autodesk Translation Framework v15.17.0.0',
/* authorisation */ '');

FILE_SCHEMA (('AUTOMOTIVE_DESIGN { 1 0 10303 214 3 1 1 }'));
ENDSEC;

DATA;
#10=MECHANICAL_DESIGN_GEOMETRIC_PRESENTATION_REPRESENTATION('',(#455),#12779);
#293=CONICAL_SURFACE('',#6730,0.275,0.785398163397449);
#387=SHAPE_REPRESENTATION_RELATIONSHIP('SRR','None',#12933,#421);
#421=ADVANCED_BREP_SHAPE_REPRESENTATION('',(#497),#12750);
#455=STYLED_ITEM('',(#13191),#497);
#497=MANIFOLD_SOLID_BREP('Body1',#6189);
#556=FACE_BOUND('',#1305,.T.);
#557=FACE_BOUND('',#1308,.T.);
#708=PLANE('',#6735);
#709=PLANE('',#6739);
#906=FACE_OUTER_BOUND('',#1302,.T.);
#907=FACE_OUTER_BOUND('',#1303,.T.);
#908=FACE_OUTER_BOUND('',#1304,.T.);
#909=FACE_OUTER_BOUND('',#1306,.T.);
#910=FACE_OUTER_BOUND('',#1307,.T.);
#1302=EDGE_LOOP('',(#4360,#4361,#4362,#4363));
#1303=EDGE_LOOP('',(#4364,#4365,#4366,#4367));
#1304=EDGE_LOOP('',(#4368));
#1305=EDGE_LOOP('',(#4369));
#1306=EDGE_LOOP('',(#4370,#4371,#4372,#4373));
#1307=EDGE_LOOP('',(#4374));
#1308=EDGE_LOOP('',(#4375));
#1783=LINE('',#10456,#2132);
#1784=LINE('',#10460,#2133);
#1785=LINE('',#10467,#2134);
#2132=VECTOR('',#7769,0.275);
#2133=VECTOR('',#7774,0.265);
#2134=VECTOR('',#7783,0.5);
#2453=CIRCLE('',#6731,0.285);
#2454=CIRCLE('',#6732,0.265);
#2455=CIRCLE('',#6734,0.265);
#2456=CIRCLE('',#6736,0.5);
#2457=CIRCLE('',#6738,0.5);
#2858=VERTEX_POINT('',#10453);
#2859=VERTEX_POINT('',#10455);
#2860=VERTEX_POINT('',#10459);
#2861=VERTEX_POINT('',#10463);
#2862=VERTEX_POINT('',#10466);
#3435=EDGE_CURVE('',#2858,#2858,#2453,.T.);
#3436=EDGE_CURVE('',#2858,#2859,#1783,.T.);
#3437=EDGE_CURVE('',#2859,#2859,#2454,.T.);
#3438=EDGE_CURVE('',#2859,#2860,#1784,.T.);
#3439=EDGE_CURVE('',#2860,#2860,#2455,.T.);
#3440=EDGE_CURVE('',#2861,#2861,#2456,.T.);
#3441=EDGE_CURVE('',#2861,#2862,#1785,.T.);
#3442=EDGE_CURVE('',#2862,#2862,#2457,.T.);
#4360=ORIENTED_EDGE('',*,*,#3435,.T.);
#4361=ORIENTED_EDGE('',*,*,#3436,.T.);
#4362=ORIENTED_EDGE('',*,*,#3437,.T.);
#4363=ORIENTED_EDGE('',*,*,#3436,.F.);
#4364=ORIENTED_EDGE('',*,*,#3437,.F.);
#4365=ORIENTED_EDGE('',*,*,#3438,.T.);
#4366=ORIENTED_EDGE('',*,*,#3439,.T.);
#4367=ORIENTED_EDGE('',*,*,#3438,.F.);
#4368=ORIENTED_EDGE('',*,*,#3440,.T.);
#4369=ORIENTED_EDGE('',*,*,#3435,.F.);
#4370=ORIENTED_EDGE('',*,*,#3440,.F.);
#4371=ORIENTED_EDGE('',*,*,#3441,.T.);
#4372=ORIENTED_EDGE('',*,*,#3442,.T.);
#4373=ORIENTED_EDGE('',*,*,#3441,.F.);
#4374=ORIENTED_EDGE('',*,*,#3442,.F.);
#4375=ORIENTED_EDGE('',*,*,#3439,.F.);
#5685=CYLINDRICAL_SURFACE('',#6733,0.265);
#5686=CYLINDRICAL_SURFACE('',#6737,0.5);
#5883=ADVANCED_FACE('',(#906),#293,.F.);
#5884=ADVANCED_FACE('',(#907),#5685,.F.);
#5885=ADVANCED_FACE('',(#908,#556),#708,.T.);
#5886=ADVANCED_FACE('',(#909),#5686,.T.);
#5887=ADVANCED_FACE('',(#910,#557),#709,.F.);
#6189=CLOSED_SHELL('',(#5883,#5884,#5885,#5886,#5887));
#6729=AXIS2_PLACEMENT_3D('',#10451,#7763,#7764);
#6730=AXIS2_PLACEMENT_3D('',#10452,#7765,#7766);
#6731=AXIS2_PLACEMENT_3D('',#10454,#7767,#7768);
#6732=AXIS2_PLACEMENT_3D('',#10457,#7770,#7771);
#6733=AXIS2_PLACEMENT_3D('',#10458,#7772,#7773);
#6734=AXIS2_PLACEMENT_3D('',#10461,#7775,#7776);
#6735=AXIS2_PLACEMENT_3D('',#10462,#7777,#7778);
#6736=AXIS2_PLACEMENT_3D('',#10464,#7779,#7780);
#6737=AXIS2_PLACEMENT_3D('',#10465,#7781,#7782);
#6738=AXIS2_PLACEMENT_3D('',#10468,#7784,#7785);
#6739=AXIS2_PLACEMENT_3D('',#10469,#7786,#7787);
#7763=DIRECTION('axis',(0.,0.,1.));
#7764=DIRECTION('refdir',(1.,0.,0.));
#7765=DIRECTION('center_axis',(0.,1.,0.));
#7766=DIRECTION('ref_axis',(1.,0.,0.));
#7767=DIRECTION('center_axis',(0.,1.,0.));
#7768=DIRECTION('ref_axis',(1.,0.,0.));
#7769=DIRECTION('',(0.707106781186548,-0.707106781186547,-8.65956056235494E-17));
#7770=DIRECTION('center_axis',(0.,-1.,0.));
#7771=DIRECTION('ref_axis',(1.,0.,0.));
#7772=DIRECTION('center_axis',(0.,1.,0.));
#7773=DIRECTION('ref_axis',(1.,0.,0.));
#7774=DIRECTION('',(0.,-1.,0.));
#7775=DIRECTION('center_axis',(0.,-1.,0.));
#7776=DIRECTION('ref_axis',(1.,0.,0.));
#7777=DIRECTION('center_axis',(0.,1.,0.));
#7778=DIRECTION('ref_axis',(1.,0.,0.));
#7779=DIRECTION('center_axis',(0.,1.,0.));
#7780=DIRECTION('ref_axis',(1.,0.,0.));
#7781=DIRECTION('center_axis',(0.,1.,0.));
#7782=DIRECTION('ref_axis',(1.,0.,0.));
#7783=DIRECTION('',(0.,-1.,0.));
#7784=DIRECTION('center_axis',(0.,1.,0.));
#7785=DIRECTION('ref_axis',(1.,0.,0.));
#7786=DIRECTION('center_axis',(0.,1.,0.));
#7787=DIRECTION('ref_axis',(1.,0.,0.));
#10451=CARTESIAN_POINT('',(0.,0.,0.));
#10452=CARTESIAN_POINT('Origin',(0.,0.09,0.));
#10453=CARTESIAN_POINT('',(-0.285,0.1,3.49024337756996E-17));
#10454=CARTESIAN_POINT('Origin',(0.,0.1,0.));
#10455=CARTESIAN_POINT('',(-0.265,0.08,-3.24531401774049E-17));
#10456=CARTESIAN_POINT('',(-0.275,0.09,3.36777869765522E-17));
#10457=CARTESIAN_POINT('Origin',(0.,0.08,0.));
#10458=CARTESIAN_POINT('Origin',(0.,0.,0.));
#10459=CARTESIAN_POINT('',(-0.265,0.,3.24531401774049E-17));
#10460=CARTESIAN_POINT('',(-0.265,0.,3.24531401774049E-17));
#10461=CARTESIAN_POINT('Origin',(0.,0.,0.));
#10462=CARTESIAN_POINT('Origin',(0.,0.1,0.));
#10463=CARTESIAN_POINT('',(-0.5,0.1,6.12323399573677E-17));
#10464=CARTESIAN_POINT('Origin',(0.,0.1,0.));
#10465=CARTESIAN_POINT('Origin',(0.,0.,0.));
#10466=CARTESIAN_POINT('',(-0.5,0.,6.12323399573677E-17));
#10467=CARTESIAN_POINT('',(-0.5,0.,6.12323399573677E-17));
#10468=CARTESIAN_POINT('Origin',(0.,0.,0.));
#10469=CARTESIAN_POINT('Origin',(0.,0.,0.));
#12710=UNCERTAINTY_MEASURE_WITH_UNIT(LENGTH_MEASURE(0.001),#12780,
'DISTANCE_ACCURACY_VALUE',
'Maximum model space distance between geometric entities at asserted c
onnectivities');
#12739=UNCERTAINTY_MEASURE_WITH_UNIT(LENGTH_MEASURE(0.001),#12780,
'DISTANCE_ACCURACY_VALUE',
'Maximum model space distance between geometric entities at asserted c
onnectivities');
#12750=(
GEOMETRIC_REPRESENTATION_CONTEXT(3)
GLOBAL_UNCERTAINTY_ASSIGNED_CONTEXT((#12710))
GLOBAL_UNIT_ASSIGNED_CONTEXT((#12780,#12782,#12783))
REPRESENTATION_CONTEXT('','3D')
);
#12779=(
GEOMETRIC_REPRESENTATION_CONTEXT(3)
GLOBAL_UNCERTAINTY_ASSIGNED_CONTEXT((#12739))
GLOBAL_UNIT_ASSIGNED_CONTEXT((#12780,#12782,#12783))
REPRESENTATION_CONTEXT('','3D')
);
#12780=(
LENGTH_UNIT()
NAMED_UNIT(*)
SI_UNIT(.CENTI.,.METRE.)
);
#12782=(
NAMED_UNIT(*)
PLANE_ANGLE_UNIT()
SI_UNIT($,.RADIAN.)
);
#12783=(
NAMED_UNIT(*)
SI_UNIT($,.STERADIAN.)
SOLID_ANGLE_UNIT()
);
#12794=SHAPE_DEFINITION_REPRESENTATION(#12833,#12933);
#12833=PRODUCT_DEFINITION_SHAPE('',$,#12973);
#12933=SHAPE_REPRESENTATION('',(#6729),#12750);
#12962=PRODUCT_DEFINITION_CONTEXT('part definition',#13081,'design');
#12973=PRODUCT_DEFINITION('Flat Washer - M5','Flat Washer - M5',#13012,
#12962);
#13012=PRODUCT_DEFINITION_FORMATION('',$,#13093);
#13081=APPLICATION_CONTEXT(
'Core Data for Automotive Mechanical Design Process');
#13082=PRODUCT_CONTEXT('part definition',#13081,'mechanical');
#13093=PRODUCT('Flat Washer - M5','Flat Washer - M5','Flat Washer - M5',
(#13082));
#13185=COLOUR_RGB('Black',0.12,0.14,0.17);
#13186=FILL_AREA_STYLE_COLOUR('',#13185);
#13187=FILL_AREA_STYLE('',(#13186));
#13188=SURFACE_STYLE_FILL_AREA(#13187);
#13189=SURFACE_SIDE_STYLE('',(#13188));
#13190=SURFACE_STYLE_USAGE(.BOTH.,#13189);
#13191=PRESENTATION_STYLE_ASSIGNMENT((#13190));
ENDSEC;
END-ISO-10303-21;
